ISO-10303-21;
HEADER;
/* Generated by software containing ST-Developer
 * from STEP Tools, Inc. (www.steptools.com) 
 */

FILE_DESCRIPTION(
/* description */ ('Hook toggle clamp'),
/* implementation_level */ '2;1');

FILE_NAME(
/* name */ 'Flat Washer - M6.step',
/* time_stamp */ '2026-10-27T21:56:56-07:00',
/* author */ (''),
/* organization */ (''),
/* preprocessor_version */ 'ST-DEVELOPER v20.2',
/* originating_system */ 'Autodesk Translation Framework v15.17.0.0',
/* authorisation */ '');

FILE_SCHEMA (('AUTOMOTIVE_DESIGN { 1 0 10303 214 3 1 1 }'));
ENDSEC;

DATA;
#10=MECHANICAL_DESIGN_GEOMETRIC_PRESENTATION_REPRESENTATION('',(#201),#5458);
#167=SHAPE_REPRESENTATION_RELATIONSHIP('SRR','None',#5551,#184);
#184=ADVANCED_BREP_SHAPE_REPRESENTATION('',(#217),#5453);
#201=STYLED_ITEM('',(#5724),#217);
#217=MANIFOLD_SOLID_BREP('Body1',#2983);
#271=FACE_BOUND('',#762,.T.);
#272=FACE_BOUND('',#764,.T.);
#376=PLANE('',#3434);
#377=PLANE('',#3435);
#537=FACE_OUTER_BOUND('',#759,.T.);
#538=FACE_OUTER_BOUND('',#760,.T.);
#539=FACE_OUTER_BOUND('',#761,.T.);
#540=FACE_OUTER_BOUND('',#763,.T.);
#759=EDGE_LOOP('',(#2633,#2634,#2635,#2636));
#760=EDGE_LOOP('',(#2637,#2638,#2639,#2640));
#761=EDGE_LOOP('',(#2641));
#762=EDGE_LOOP('',(#2642));
#763=EDGE_LOOP('',(#2643));
#764=EDGE_LOOP('',(#2644));
#1012=LINE('',#5188,#1249);
#1013=LINE('',#5194,#1250);
#1249=VECTOR('',#4236,0.32);
#1250=VECTOR('',#4243,0.6);
#1358=CIRCLE('',#3429,0.32);
#1359=CIRCLE('',#3430,0.32);
#1360=CIRCLE('',#3432,0.6);
#1361=CIRCLE('',#3433,0.6);
#1589=VERTEX_POINT('',#5185);
#1590=VERTEX_POINT('',#5187);
#1591=VERTEX_POINT('',#5191);
#1592=VERTEX_POINT('',#5193);
#1943=EDGE_CURVE('',#1589,#1589,#1358,.T.);
#1944=EDGE_CURVE('',#1589,#1590,#1012,.T.);
#1945=EDGE_CURVE('',#1590,#1590,#1359,.T.);
#1946=EDGE_CURVE('',#1591,#1591,#1360,.T.);
#1947=EDGE_CURVE('',#1591,#1592,#1013,.T.);
#1948=EDGE_CURVE('',#1592,#1592,#1361,.T.);
#2633=ORIENTED_EDGE('',*,*,#1943,.F.);
#2634=ORIENTED_EDGE('',*,*,#1944,.T.);
#2635=ORIENTED_EDGE('',*,*,#1945,.T.);
#2636=ORIENTED_EDGE('',*,*,#1944,.F.);
#2637=ORIENTED_EDGE('',*,*,#1946,.F.);
#2638=ORIENTED_EDGE('',*,*,#1947,.T.);
#2639=ORIENTED_EDGE('',*,*,#1948,.T.);
#2640=ORIENTED_EDGE('',*,*,#1947,.F.);
#2641=ORIENTED_EDGE('',*,*,#1946,.T.);
#2642=ORIENTED_EDGE('',*,*,#1943,.T.);
#2643=ORIENTED_EDGE('',*,*,#1948,.F.);
#2644=ORIENTED_EDGE('',*,*,#1945,.F.);
#2789=CYLINDRICAL_SURFACE('',#3428,0.32);
#2790=CYLINDRICAL_SURFACE('',#3431,0.6);
#2941=ADVANCED_FACE('',(#537),#2789,.F.);
#2942=ADVANCED_FACE('',(#538),#2790,.T.);
#2943=ADVANCED_FACE('',(#539,#271),#376,.T.);
#2944=ADVANCED_FACE('',(#540,#272),#377,.F.);
#2983=CLOSED_SHELL('',(#2941,#2942,#2943,#2944));
#3427=AXIS2_PLACEMENT_3D('',#5183,#4230,#4231);
#3428=AXIS2_PLACEMENT_3D('',#5184,#4232,#4233);
#3429=AXIS2_PLACEMENT_3D('',#5186,#4234,#4235);
#3430=AXIS2_PLACEMENT_3D('',#5189,#4237,#4238);
#3431=AXIS2_PLACEMENT_3D('',#5190,#4239,#4240);
#3432=AXIS2_PLACEMENT_3D('',#5192,#4241,#4242);
#3433=AXIS2_PLACEMENT_3D('',#5195,#4244,#4245);
#3434=AXIS2_PLACEMENT_3D('',#5196,#4246,#4247);
#3435=AXIS2_PLACEMENT_3D('',#5197,#4248,#4249);
#4230=DIRECTION('axis',(0.,0.,1.));
#4231=DIRECTION('refdir',(1.,0.,0.));
#4232=DIRECTION('center_axis',(0.,1.,0.));
#4233=DIRECTION('ref_axis',(1.,0.,0.));
#4234=DIRECTION('center_axis',(0.,-1.,0.));
#4235=DIRECTION('ref_axis',(1.,0.,0.));
#4236=DIRECTION('',(0.,-1.,0.));
#4237=DIRECTION('center_axis',(0.,-1.,0.));
#4238=DIRECTION('ref_axis',(1.,0.,0.));
#4239=DIRECTION('center_axis',(0.,1.,0.));
#4240=DIRECTION('ref_axis',(1.,0.,0.));
#4241=DIRECTION('center_axis',(0.,1.,0.));
#4242=DIRECTION('ref_axis',(1.,0.,0.));
#4243=DIRECTION('',(0.,-1.,0.));
#4244=DIRECTION('center_axis',(0.,1.,0.));
#4245=DIRECTION('ref_axis',(1.,0.,0.));
#4246=DIRECTION('center_axis',(0.,1.,0.));
#4247=DIRECTION('ref_axis',(1.,0.,0.));
#4248=DIRECTION('center_axis',(0.,1.,0.));
#4249=DIRECTION('ref_axis',(1.,0.,0.));
#5183=CARTESIAN_POINT('',(0.,0.,0.));
#5184=CARTESIAN_POINT('Origin',(0.,0.,0.));
#5185=CARTESIAN_POINT('',(-0.32,0.16,3.91886975727153E-17));
#5186=CARTESIAN_POINT('Origin',(0.,0.16,0.));
#5187=CARTESIAN_POINT('',(-0.32,0.,3.91886975727153E-17));
#5188=CARTESIAN_POINT('',(-0.32,0.,3.91886975727153E-17));
#5189=CARTESIAN_POINT('Origin',(0.,0.,0.));
#5190=CARTESIAN_POINT('Origin',(0.,0.,0.));
#5191=CARTESIAN_POINT('',(-0.6,0.16,7.34788079488412E-17));
#5192=CARTESIAN_POINT('Origin',(0.,0.16,0.));
#5193=CARTESIAN_POINT('',(-0.6,0.,7.34788079488412E-17));
#5194=CARTESIAN_POINT('',(-0.6,0.,7.34788079488412E-17));
#5195=CARTESIAN_POINT('Origin',(0.,0.,0.));
#5196=CARTESIAN_POINT('Origin',(0.,0.16,0.));
#5197=CARTESIAN_POINT('Origin',(0.,0.,0.));
#5430=UNCERTAINTY_MEASURE_WITH_UNIT(LENGTH_MEASURE(0.001),#5459,
'DISTANCE_ACCURACY_VALUE',
'Maximum model space distance between geometric entities at asserted c
onnectivities');
#5435=UNCERTAINTY_MEASURE_WITH_UNIT(LENGTH_MEASURE(0.001),#5459,
'DISTANCE_ACCURACY_VALUE',
'Maximum model space distance between geometric entities at asserted c
onnectivities');
#5453=(
GEOMETRIC_REPRESENTATION_CONTEXT(3)
GLOBAL_UNCERTAINTY_ASSIGNED_CONTEXT((#5430))
GLOBAL_UNIT_ASSIGNED_CONTEXT((#5459,#5461,#5462))
REPRESENTATION_CONTEXT('','3D')
);
#5458=(
GEOMETRIC_REPRESENTATION_CONTEXT(3)
GLOBAL_UNCERTAINTY_ASSIGNED_CONTEXT((#5435))
GLOBAL_UNIT_ASSIGNED_CONTEXT((#5459,#5461,#5462))
REPRESENTATION_CONTEXT('','3D')
);
#5459=(
LENGTH_UNIT()
NAMED_UNIT(*)
SI_UNIT(.CENTI.,.METRE.)
);
#5461=(
NAMED_UNIT(*)
PLANE_ANGLE_UNIT()
SI_UNIT($,.RADIAN.)
);
#5462=(
NAMED_UNIT(*)
SI_UNIT($,.STERADIAN.)
SOLID_ANGLE_UNIT()
);
#5480=SHAPE_DEFINITION_REPRESENTATION(#5503,#5551);
#5503=PRODUCT_DEFINITION_SHAPE('',$,#5574);
#5551=SHAPE_REPRESENTATION('',(#3427),#5453);
#5556=PRODUCT_DEFINITION_CONTEXT('part definition',#5624,'design');
#5574=PRODUCT_DEFINITION('Flat Washer - M6','Flat Washer - M6',#5596,#5556);
#5596=PRODUCT_DEFINITION_FORMATION('',$,#5643);
#5624=APPLICATION_CONTEXT(
'Core Data for Automotive Mechanical Design Process');
#5625=PRODUCT_CONTEXT('part definition',#5624,'mechanical');
#5643=PRODUCT('Flat Washer - M6','Flat Washer - M6','Flat Washer - M6',
(#5625));
#5718=COLOUR_RGB('Black',0.12,0.14,0.17);
#5719=FILL_AREA_STYLE_COLOUR('',#5718);
#5720=FILL_AREA_STYLE('',(#5719));
#5721=SURFACE_STYLE_FILL_AREA(#5720);
#5722=SURFACE_SIDE_STYLE('',(#5721));
#5723=SURFACE_STYLE_USAGE(.BOTH.,#5722);
#5724=PRESENTATION_STYLE_ASSIGNMENT((#5723));
ENDSEC;
END-ISO-10303-21;
